ISO-10303-21;
HEADER;
/* Generated by software containing ST-Developer
 * from STEP Tools, Inc. (www.steptools.com) 
 */

FILE_DESCRIPTION(
/* description */ ('Rigid flange shaft coupling assembly'),
/* implementation_level */ '2;1');

FILE_NAME(
/* name */ 'Mounting bush (2).step',
/* time_stamp */ '2026-10-27T10:47:16-07:00',
/* author */ (''),
/* organization */ (''),
/* preprocessor_version */ 'ST-DEVELOPER v20.2',
/* originating_system */ 'Autodesk Translation Framework v15.17.0.0',
/* authorisation */ '');

FILE_SCHEMA (('AUTOMOTIVE_DESIGN { 1 0 10303 214 3 1 1 }'));
ENDSEC;

DATA;
#10=MECHANICAL_DESIGN_GEOMETRIC_PRESENTATION_REPRESENTATION('',(#405),#9141);
#349=SHAPE_REPRESENTATION_RELATIONSHIP('SRR','None',#9283,#377);
#377=ADVANCED_BREP_SHAPE_REPRESENTATION('',(#434),#9118);
#405=STYLED_ITEM('',(#9493),#434);
#434=MANIFOLD_SOLID_BREP('Body1',#4759);
#481=FACE_BOUND('',#1097,.T.);
#482=FACE_BOUND('',#1099,.T.);
#604=PLANE('',#5191);
#605=PLANE('',#5192);
#794=FACE_OUTER_BOUND('',#1094,.T.);
#795=FACE_OUTER_BOUND('',#1095,.T.);
#796=FACE_OUTER_BOUND('',#1096,.T.);
#797=FACE_OUTER_BOUND('',#1098,.T.);
#1094=EDGE_LOOP('',(#3459,#3460,#3461,#3462));
#1095=EDGE_LOOP('',(#3463,#3464,#3465,#3466));
#1096=EDGE_LOOP('',(#3467));
#1097=EDGE_LOOP('',(#3468));
#1098=EDGE_LOOP('',(#3469));
#1099=EDGE_LOOP('',(#3470));
#1481=LINE('',#7329,#1826);
#1482=LINE('',#7335,#1827);
#1826=VECTOR('',#5906,0.425);
#1827=VECTOR('',#5913,0.645);
#2127=CIRCLE('',#5186,0.425);
#2128=CIRCLE('',#5187,0.425);
#2129=CIRCLE('',#5189,0.645);
#2130=CIRCLE('',#5190,0.645);
#2348=VERTEX_POINT('',#7326);
#2349=VERTEX_POINT('',#7328);
#2350=VERTEX_POINT('',#7332);
#2351=VERTEX_POINT('',#7334);
#2773=EDGE_CURVE('',#2348,#2348,#2127,.T.);
#2774=EDGE_CURVE('',#2348,#2349,#1481,.T.);
#2775=EDGE_CURVE('',#2349,#2349,#2128,.T.);
#2776=EDGE_CURVE('',#2350,#2350,#2129,.T.);
#2777=EDGE_CURVE('',#2350,#2351,#1482,.T.);
#2778=EDGE_CURVE('',#2351,#2351,#2130,.T.);
#3459=ORIENTED_EDGE('',*,*,#2773,.F.);
#3460=ORIENTED_EDGE('',*,*,#2774,.T.);
#3461=ORIENTED_EDGE('',*,*,#2775,.T.);
#3462=ORIENTED_EDGE('',*,*,#2774,.F.);
#3463=ORIENTED_EDGE('',*,*,#2776,.F.);
#3464=ORIENTED_EDGE('',*,*,#2777,.T.);
#3465=ORIENTED_EDGE('',*,*,#2778,.T.);
#3466=ORIENTED_EDGE('',*,*,#2777,.F.);
#3467=ORIENTED_EDGE('',*,*,#2776,.T.);
#3468=ORIENTED_EDGE('',*,*,#2773,.T.);
#3469=ORIENTED_EDGE('',*,*,#2778,.F.);
#3470=ORIENTED_EDGE('',*,*,#2775,.F.);
#4415=CYLINDRICAL_SURFACE('',#5185,0.425);
#4416=CYLINDRICAL_SURFACE('',#5188,0.645);
#4530=ADVANCED_FACE('',(#794),#4415,.F.);
#4531=ADVANCED_FACE('',(#795),#4416,.T.);
#4532=ADVANCED_FACE('',(#796,#481),#604,.T.);
#4533=ADVANCED_FACE('',(#797,#482),#605,.F.);
#4759=CLOSED_SHELL('',(#4530,#4531,#4532,#4533));
#5184=AXIS2_PLACEMENT_3D('',#7324,#5900,#5901);
#5185=AXIS2_PLACEMENT_3D('',#7325,#5902,#5903);
#5186=AXIS2_PLACEMENT_3D('',#7327,#5904,#5905);
#5187=AXIS2_PLACEMENT_3D('',#7330,#5907,#5908);
#5188=AXIS2_PLACEMENT_3D('',#7331,#5909,#5910);
#5189=AXIS2_PLACEMENT_3D('',#7333,#5911,#5912);
#5190=AXIS2_PLACEMENT_3D('',#7336,#5914,#5915);
#5191=AXIS2_PLACEMENT_3D('',#7337,#5916,#5917);
#5192=AXIS2_PLACEMENT_3D('',#7338,#5918,#5919);
#5900=DIRECTION('axis',(0.,0.,1.));
#5901=DIRECTION('refdir',(1.,0.,0.));
#5902=DIRECTION('center_axis',(0.,0.,1.));
#5903=DIRECTION('ref_axis',(1.,0.,0.));
#5904=DIRECTION('center_axis',(0.,0.,-1.));
#5905=DIRECTION('ref_axis',(1.,0.,0.));
#5906=DIRECTION('',(0.,0.,-1.));
#5907=DIRECTION('center_axis',(0.,0.,-1.));
#5908=DIRECTION('ref_axis',(1.,0.,0.));
#5909=DIRECTION('center_axis',(0.,0.,1.));
#5910=DIRECTION('ref_axis',(1.,0.,0.));
#5911=DIRECTION('center_axis',(0.,0.,1.));
#5912=DIRECTION('ref_axis',(1.,0.,0.));
#5913=DIRECTION('',(0.,0.,-1.));
#5914=DIRECTION('center_axis',(0.,0.,1.));
#5915=DIRECTION('ref_axis',(1.,0.,0.));
#5916=DIRECTION('center_axis',(0.,0.,1.));
#5917=DIRECTION('ref_axis',(1.,0.,0.));
#5918=DIRECTION('center_axis',(0.,0.,1.));
#5919=DIRECTION('ref_axis',(1.,0.,0.));
#7324=CARTESIAN_POINT('',(0.,0.,0.));
#7325=CARTESIAN_POINT('Origin',(-4.75,20.,3.2));
#7326=CARTESIAN_POINT('',(-5.175,20.,4.4));
#7327=CARTESIAN_POINT('Origin',(-4.75,20.,4.4));
#7328=CARTESIAN_POINT('',(-5.175,20.,3.2));
#7329=CARTESIAN_POINT('',(-5.175,20.,3.2));
#7330=CARTESIAN_POINT('Origin',(-4.75,20.,3.2));
#7331=CARTESIAN_POINT('Origin',(-4.75,20.,3.2));
#7332=CARTESIAN_POINT('',(-5.395,20.,4.4));
#7333=CARTESIAN_POINT('Origin',(-4.75,20.,4.4));
#7334=CARTESIAN_POINT('',(-5.395,20.,3.2));
#7335=CARTESIAN_POINT('',(-5.395,20.,3.2));
#7336=CARTESIAN_POINT('Origin',(-4.75,20.,3.2));
#7337=CARTESIAN_POINT('Origin',(-4.75,20.,4.4));
#7338=CARTESIAN_POINT('Origin',(-4.75,20.,3.2));
#9085=UNCERTAINTY_MEASURE_WITH_UNIT(LENGTH_MEASURE(0.001),#9142,
'DISTANCE_ACCURACY_VALUE',
'Maximum model space distance between geometric entities at asserted c
onnectivities');
#9108=UNCERTAINTY_MEASURE_WITH_UNIT(LENGTH_MEASURE(0.001),#9142,
'DISTANCE_ACCURACY_VALUE',
'Maximum model space distance between geometric entities at asserted c
onnectivities');
#9118=(
GEOMETRIC_REPRESENTATION_CONTEXT(3)
GLOBAL_UNCERTAINTY_ASSIGNED_CONTEXT((#9085))
GLOBAL_UNIT_ASSIGNED_CONTEXT((#9142,#9144,#9145))
REPRESENTATION_CONTEXT('','3D')
);
#9141=(
GEOMETRIC_REPRESENTATION_CONTEXT(3)
GLOBAL_UNCERTAINTY_ASSIGNED_CONTEXT((#9108))
GLOBAL_UNIT_ASSIGNED_CONTEXT((#9142,#9144,#9145))
REPRESENTATION_CONTEXT('','3D')
);
#9142=(
LENGTH_UNIT()
NAMED_UNIT(*)
SI_UNIT(.CENTI.,.METRE.)
);
#9144=(
NAMED_UNIT(*)
PLANE_ANGLE_UNIT()
SI_UNIT($,.RADIAN.)
);
#9145=(
NAMED_UNIT(*)
SI_UNIT($,.STERADIAN.)
SOLID_ANGLE_UNIT()
);
#9155=SHAPE_DEFINITION_REPRESENTATION(#9187,#9283);
#9187=PRODUCT_DEFINITION_SHAPE('',$,#9316);
#9283=SHAPE_REPRESENTATION('',(#5184),#9118);
#9306=PRODUCT_DEFINITION_CONTEXT('part definition',#9404,'design');
#9316=PRODUCT_DEFINITION('Mounting bush (2)','Mounting bush (2)',#9348,#9306);
#9348=PRODUCT_DEFINITION_FORMATION('',$,#9415);
#9404=APPLICATION_CONTEXT(
'Core Data for Automotive Mechanical Design Process');
#9405=PRODUCT_CONTEXT('part definition',#9404,'mechanical');
#9415=PRODUCT('Mounting bush (2)','Mounting bush (2)','Mounting bush (2)',(#9405));
#9487=COLOUR_RGB('Sky Blue',0.24,0.69,0.87);
#9488=FILL_AREA_STYLE_COLOUR('',#9487);
#9489=FILL_AREA_STYLE('',(#9488));
#9490=SURFACE_STYLE_FILL_AREA(#9489);
#9491=SURFACE_SIDE_STYLE('',(#9490));
#9492=SURFACE_STYLE_USAGE(.BOTH.,#9491);
#9493=PRESENTATION_STYLE_ASSIGNMENT((#9492));
ENDSEC;
END-ISO-10303-21;
